ISO-10303-21;
HEADER;
/* Generated by software containing ST-Developer
 * from STEP Tools, Inc. (www.steptools.com) 
 */

FILE_DESCRIPTION(
/* description */ ('Gear mesh backlash fixture'),
/* implementation_level */ '2;1');

FILE_NAME(
/* name */ 'M5x14 Cap Screw.step',
/* time_stamp */ '2026-10-28T03:26:00-07:00',
/* author */ (''),
/* organization */ (''),
/* preprocessor_version */ 'ST-DEVELOPER v20.2',
/* originating_system */ 'Autodesk Translation Framework v15.17.0.0',
/* authorisation */ '');

FILE_SCHEMA (('AUTOMOTIVE_DESIGN { 1 0 10303 214 3 1 1 }'));
ENDSEC;

DATA;
#10=MECHANICAL_DESIGN_GEOMETRIC_PRESENTATION_REPRESENTATION('',(#1050),#57900);
#372=ORIENTED_CLOSED_SHELL('',*,#13611,.F.);
#375=BREP_WITH_VOIDS('Body1',#13612,(#372));
#769=CONICAL_SURFACE('',#14896,0.4,0.785398163397448);
#770=CONICAL_SURFACE('',#14900,0.41,0.785398163397448);
#771=CONICAL_SURFACE('',#14904,0.26,0.463647609000806);
#943=SHAPE_REPRESENTATION_RELATIONSHIP('SRR','None',#58141,#993);
#993=ADVANCED_BREP_SHAPE_REPRESENTATION('',(#375),#57874);
#1050=STYLED_ITEM('',(#58472),#375);
#1281=FACE_BOUND('',#2945,.T.);
#1521=PLANE('',#14884);
#1522=PLANE('',#14885);
#1523=PLANE('',#14886);
#1524=PLANE('',#14887);
#1525=PLANE('',#14888);
#1526=PLANE('',#14889);
#1527=PLANE('',#14890);
#1528=PLANE('',#14891);
#1529=PLANE('',#14892);
#1530=PLANE('',#14894);
#1531=PLANE('',#14902);
#2028=FACE_OUTER_BOUND('',#2931,.T.);
#2029=FACE_OUTER_BOUND('',#2932,.T.);
#2030=FACE_OUTER_BOUND('',#2933,.T.);
#2031=FACE_OUTER_BOUND('',#2934,.T.);
#2032=FACE_OUTER_BOUND('',#2935,.T.);
#2033=FACE_OUTER_BOUND('',#2936,.T.);
#2034=FACE_OUTER_BOUND('',#2937,.T.);
#2035=FACE_OUTER_BOUND('',#2938,.T.);
#2036=FACE_OUTER_BOUND('',#2939,.T.);
#2037=FACE_OUTER_BOUND('',#2940,.T.);
#2038=FACE_OUTER_BOUND('',#2941,.T.);
#2039=FACE_OUTER_BOUND('',#2942,.T.);
#2040=FACE_OUTER_BOUND('',#2943,.T.);
#2041=FACE_OUTER_BOUND('',#2944,.T.);
#2042=FACE_OUTER_BOUND('',#2946,.T.);
#2043=FACE_OUTER_BOUND('',#2947,.T.);
#2931=EDGE_LOOP('',(#10415,#10416,#10417,#10418));
#2932=EDGE_LOOP('',(#10419,#10420,#10421,#10422));
#2933=EDGE_LOOP('',(#10423,#10424,#10425,#10426));
#2934=EDGE_LOOP('',(#10427,#10428,#10429,#10430));
#2935=EDGE_LOOP('',(#10431,#10432,#10433,#10434));
#2936=EDGE_LOOP('',(#10435,#10436,#10437,#10438));
#2937=EDGE_LOOP('',(#10439,#10440,#10441,#10442,#10443,#10444));
#2938=EDGE_LOOP('',(#10445,#10446,#10447,#10448,#10449,#10450));
#2939=EDGE_LOOP('',(#10451));
#2940=EDGE_LOOP('',(#10452));
#2941=EDGE_LOOP('',(#10453,#10454,#10455,#10456));
#2942=EDGE_LOOP('',(#10457,#10458,#10459,#10460));
#2943=EDGE_LOOP('',(#10461,#10462,#10463,#10464));
#2944=EDGE_LOOP('',(#10465));
#2945=EDGE_LOOP('',(#10466));
#2946=EDGE_LOOP('',(#10467,#10468,#10469,#10470));
#2947=EDGE_LOOP('',(#10471,#10472,#10473,#10474));
#3840=LINE('',#21350,#4729);
#3841=LINE('',#21352,#4730);
#3842=LINE('',#21354,#4731);
#3843=LINE('',#21355,#4732);
#3844=LINE('',#21358,#4733);
#3845=LINE('',#21360,#4734);
#3846=LINE('',#21361,#4735);
#3847=LINE('',#21364,#4736);
#3848=LINE('',#21366,#4737);
#3849=LINE('',#21367,#4738);
#3850=LINE('',#21370,#4739);
#3851=LINE('',#21372,#4740);
#3852=LINE('',#21373,#4741);
#3853=LINE('',#21376,#4742);
#3854=LINE('',#21378,#4743);
#3855=LINE('',#21379,#4744);
#3856=LINE('',#21381,#4745);
#3857=LINE('',#21382,#4746);
#3858=LINE('',#21394,#4747);
#3859=LINE('',#21398,#4748);
#3860=LINE('',#21402,#4749);
#3861=LINE('',#21409,#4750);
#3862=LINE('',#21411,#4751);
#4729=VECTOR('',#17387,1.);
#4730=VECTOR('',#17388,1.);
#4731=VECTOR('',#17389,1.);
#4732=VECTOR('',#17390,1.);
#4733=VECTOR('',#17393,1.);
#4734=VECTOR('',#17394,1.);
#4735=VECTOR('',#17395,1.);
#4736=VECTOR('',#17398,1.);
#4737=VECTOR('',#17399,1.);
#4738=VECTOR('',#17400,1.);
#4739=VECTOR('',#17403,1.);
#4740=VECTOR('',#17404,1.);
#4741=VECTOR('',#17405,1.);
#4742=VECTOR('',#17408,1.);
#4743=VECTOR('',#17409,1.);
#4744=VECTOR('',#17410,1.);
#4745=VECTOR('',#17413,1.);
#4746=VECTOR('',#17414,1.);
#4747=VECTOR('',#17431,0.4);
#4748=VECTOR('',#17436,0.425);
#4749=VECTOR('',#17441,0.41);
#4750=VECTOR('',#17450,0.26);
#4751=VECTOR('',#17453,0.25);
#5503=CIRCLE('',#14893,0.24505);
#5504=CIRCLE('',#14895,0.375);
#5505=CIRCLE('',#14897,0.425);
#5506=CIRCLE('',#14899,0.425);
#5507=CIRCLE('',#14901,0.395);
#5508=CIRCLE('',#14903,0.27);
#5509=CIRCLE('',#14905,0.24505);
#6295=VERTEX_POINT('',#21348);
#6296=VERTEX_POINT('',#21349);
#6297=VERTEX_POINT('',#21351);
#6298=VERTEX_POINT('',#21353);
#6299=VERTEX_POINT('',#21357);
#6300=VERTEX_POINT('',#21359);
#6301=VERTEX_POINT('',#21363);
#6302=VERTEX_POINT('',#21365);
#6303=VERTEX_POINT('',#21369);
#6304=VERTEX_POINT('',#21371);
#6305=VERTEX_POINT('',#21375);
#6306=VERTEX_POINT('',#21377);
#6307=VERTEX_POINT('',#21386);
#6308=VERTEX_POINT('',#21389);
#6309=VERTEX_POINT('',#21392);
#6310=VERTEX_POINT('',#21396);
#6311=VERTEX_POINT('',#21400);
#6312=VERTEX_POINT('',#21404);
#6313=VERTEX_POINT('',#21407);
#7794=EDGE_CURVE('',#6295,#6296,#3840,.T.);
#7795=EDGE_CURVE('',#6296,#6297,#3841,.T.);
#7796=EDGE_CURVE('',#6297,#6298,#3842,.T.);
#7797=EDGE_CURVE('',#6295,#6298,#3843,.T.);
#7798=EDGE_CURVE('',#6296,#6299,#3844,.T.);
#7799=EDGE_CURVE('',#6299,#6300,#3845,.T.);
#7800=EDGE_CURVE('',#6300,#6297,#3846,.T.);
#7801=EDGE_CURVE('',#6299,#6301,#3847,.T.);
#7802=EDGE_CURVE('',#6301,#6302,#3848,.T.);
#7803=EDGE_CURVE('',#6302,#6300,#3849,.T.);
#7804=EDGE_CURVE('',#6301,#6303,#3850,.T.);
#7805=EDGE_CURVE('',#6303,#6304,#3851,.T.);
#7806=EDGE_CURVE('',#6304,#6302,#3852,.T.);
#7807=EDGE_CURVE('',#6303,#6305,#3853,.T.);
#7808=EDGE_CURVE('',#6305,#6306,#3854,.T.);
#7809=EDGE_CURVE('',#6306,#6304,#3855,.T.);
#7810=EDGE_CURVE('',#6305,#6295,#3856,.T.);
#7811=EDGE_CURVE('',#6298,#6306,#3857,.T.);
#7812=EDGE_CURVE('',#6307,#6307,#5503,.T.);
#7813=EDGE_CURVE('',#6308,#6308,#5504,.T.);
#7814=EDGE_CURVE('',#6309,#6309,#5505,.T.);
#7815=EDGE_CURVE('',#6309,#6308,#3858,.T.);
#7816=EDGE_CURVE('',#6310,#6310,#5506,.T.);
#7817=EDGE_CURVE('',#6310,#6309,#3859,.T.);
#7818=EDGE_CURVE('',#6311,#6311,#5507,.T.);
#7819=EDGE_CURVE('',#6311,#6310,#3860,.T.);
#7820=EDGE_CURVE('',#6312,#6312,#5508,.T.);
#7821=EDGE_CURVE('',#6313,#6313,#5509,.F.);
#7822=EDGE_CURVE('',#6313,#6312,#3861,.T.);
#7823=EDGE_CURVE('',#6307,#6313,#3862,.T.);
#10415=ORIENTED_EDGE('',*,*,#7794,.T.);
#10416=ORIENTED_EDGE('',*,*,#7795,.T.);
#10417=ORIENTED_EDGE('',*,*,#7796,.T.);
#10418=ORIENTED_EDGE('',*,*,#7797,.F.);
#10419=ORIENTED_EDGE('',*,*,#7798,.T.);
#10420=ORIENTED_EDGE('',*,*,#7799,.T.);
#10421=ORIENTED_EDGE('',*,*,#7800,.T.);
#10422=ORIENTED_EDGE('',*,*,#7795,.F.);
#10423=ORIENTED_EDGE('',*,*,#7801,.T.);
#10424=ORIENTED_EDGE('',*,*,#7802,.T.);
#10425=ORIENTED_EDGE('',*,*,#7803,.T.);
#10426=ORIENTED_EDGE('',*,*,#7799,.F.);
#10427=ORIENTED_EDGE('',*,*,#7804,.T.);
#10428=ORIENTED_EDGE('',*,*,#7805,.T.);
#10429=ORIENTED_EDGE('',*,*,#7806,.T.);
#10430=ORIENTED_EDGE('',*,*,#7802,.F.);
#10431=ORIENTED_EDGE('',*,*,#7807,.T.);
#10432=ORIENTED_EDGE('',*,*,#7808,.T.);
#10433=ORIENTED_EDGE('',*,*,#7809,.T.);
#10434=ORIENTED_EDGE('',*,*,#7805,.F.);
#10435=ORIENTED_EDGE('',*,*,#7810,.T.);
#10436=ORIENTED_EDGE('',*,*,#7797,.T.);
#10437=ORIENTED_EDGE('',*,*,#7811,.T.);
#10438=ORIENTED_EDGE('',*,*,#7808,.F.);
#10439=ORIENTED_EDGE('',*,*,#7810,.F.);
#10440=ORIENTED_EDGE('',*,*,#7807,.F.);
#10441=ORIENTED_EDGE('',*,*,#7804,.F.);
#10442=ORIENTED_EDGE('',*,*,#7801,.F.);
#10443=ORIENTED_EDGE('',*,*,#7798,.F.);
#10444=ORIENTED_EDGE('',*,*,#7794,.F.);
#10445=ORIENTED_EDGE('',*,*,#7811,.F.);
#10446=ORIENTED_EDGE('',*,*,#7796,.F.);
#10447=ORIENTED_EDGE('',*,*,#7800,.F.);
#10448=ORIENTED_EDGE('',*,*,#7803,.F.);
#10449=ORIENTED_EDGE('',*,*,#7806,.F.);
#10450=ORIENTED_EDGE('',*,*,#7809,.F.);
#10451=ORIENTED_EDGE('',*,*,#7812,.F.);
#10452=ORIENTED_EDGE('',*,*,#7813,.F.);
#10453=ORIENTED_EDGE('',*,*,#7814,.F.);
#10454=ORIENTED_EDGE('',*,*,#7815,.T.);
#10455=ORIENTED_EDGE('',*,*,#7813,.T.);
#10456=ORIENTED_EDGE('',*,*,#7815,.F.);
#10457=ORIENTED_EDGE('',*,*,#7816,.F.);
#10458=ORIENTED_EDGE('',*,*,#7817,.T.);
#10459=ORIENTED_EDGE('',*,*,#7814,.T.);
#10460=ORIENTED_EDGE('',*,*,#7817,.F.);
#10461=ORIENTED_EDGE('',*,*,#7818,.F.);
#10462=ORIENTED_EDGE('',*,*,#7819,.T.);
#10463=ORIENTED_EDGE('',*,*,#7816,.T.);
#10464=ORIENTED_EDGE('',*,*,#7819,.F.);
#10465=ORIENTED_EDGE('',*,*,#7818,.T.);
#10466=ORIENTED_EDGE('',*,*,#7820,.F.);
#10467=ORIENTED_EDGE('',*,*,#7821,.F.);
#10468=ORIENTED_EDGE('',*,*,#7822,.T.);
#10469=ORIENTED_EDGE('',*,*,#7820,.T.);
#10470=ORIENTED_EDGE('',*,*,#7822,.F.);
#10471=ORIENTED_EDGE('',*,*,#7812,.T.);
#10472=ORIENTED_EDGE('',*,*,#7823,.T.);
#10473=ORIENTED_EDGE('',*,*,#7821,.T.);
#10474=ORIENTED_EDGE('',*,*,#7823,.F.);
#12702=CYLINDRICAL_SURFACE('',#14898,0.425);
#12703=CYLINDRICAL_SURFACE('',#14906,0.24505);
#13145=ADVANCED_FACE('',(#2028),#1521,.F.);
#13146=ADVANCED_FACE('',(#2029),#1522,.F.);
#13147=ADVANCED_FACE('',(#2030),#1523,.F.);
#13148=ADVANCED_FACE('',(#2031),#1524,.F.);
#13149=ADVANCED_FACE('',(#2032),#1525,.F.);
#13150=ADVANCED_FACE('',(#2033),#1526,.F.);
#13151=ADVANCED_FACE('',(#2034),#1527,.F.);
#13152=ADVANCED_FACE('',(#2035),#1528,.F.);
#13153=ADVANCED_FACE('',(#2036),#1529,.F.);
#13154=ADVANCED_FACE('',(#2037),#1530,.T.);
#13155=ADVANCED_FACE('',(#2038),#769,.T.);
#13156=ADVANCED_FACE('',(#2039),#12702,.T.);
#13157=ADVANCED_FACE('',(#2040),#770,.T.);
#13158=ADVANCED_FACE('',(#2041,#1281),#1531,.T.);
#13159=ADVANCED_FACE('',(#2042),#771,.T.);
#13160=ADVANCED_FACE('',(#2043),#12703,.T.);
#13611=CLOSED_SHELL('',(#13145,#13146,#13147,#13148,#13149,#13150,#13151,
#13152));
#13612=CLOSED_SHELL('',(#13153,#13154,#13155,#13156,#13157,#13158,#13159,
#13160));
#14883=AXIS2_PLACEMENT_3D('',#21346,#17383,#17384);
#14884=AXIS2_PLACEMENT_3D('',#21347,#17385,#17386);
#14885=AXIS2_PLACEMENT_3D('',#21356,#17391,#17392);
#14886=AXIS2_PLACEMENT_3D('',#21362,#17396,#17397);
#14887=AXIS2_PLACEMENT_3D('',#21368,#17401,#17402);
#14888=AXIS2_PLACEMENT_3D('',#21374,#17406,#17407);
#14889=AXIS2_PLACEMENT_3D('',#21380,#17411,#17412);
#14890=AXIS2_PLACEMENT_3D('',#21383,#17415,#17416);
#14891=AXIS2_PLACEMENT_3D('',#21384,#17417,#17418);
#14892=AXIS2_PLACEMENT_3D('',#21385,#17419,#17420);
#14893=AXIS2_PLACEMENT_3D('',#21387,#17421,#17422);
#14894=AXIS2_PLACEMENT_3D('',#21388,#17423,#17424);
#14895=AXIS2_PLACEMENT_3D('',#21390,#17425,#17426);
#14896=AXIS2_PLACEMENT_3D('',#21391,#17427,#17428);
#14897=AXIS2_PLACEMENT_3D('',#21393,#17429,#17430);
#14898=AXIS2_PLACEMENT_3D('',#21395,#17432,#17433);
#14899=AXIS2_PLACEMENT_3D('',#21397,#17434,#17435);
#14900=AXIS2_PLACEMENT_3D('',#21399,#17437,#17438);
#14901=AXIS2_PLACEMENT_3D('',#21401,#17439,#17440);
#14902=AXIS2_PLACEMENT_3D('',#21403,#17442,#17443);
#14903=AXIS2_PLACEMENT_3D('',#21405,#17444,#17445);
#14904=AXIS2_PLACEMENT_3D('',#21406,#17446,#17447);
#14905=AXIS2_PLACEMENT_3D('',#21408,#17448,#17449);
#14906=AXIS2_PLACEMENT_3D('',#21410,#17451,#17452);
#17383=DIRECTION('axis',(0.,0.,1.));
#17384=DIRECTION('refdir',(1.,0.,0.));
#17385=DIRECTION('center_axis',(0.866025403784439,0.,-0.5));
#17386=DIRECTION('ref_axis',(0.5,0.,0.866025403784439));
#17387=DIRECTION('',(-0.5,0.,-0.866025403784439));
#17388=DIRECTION('',(0.,-1.,0.));
#17389=DIRECTION('',(0.5,0.,0.866025403784439));
#17390=DIRECTION('',(0.,-1.,0.));
#17391=DIRECTION('center_axis',(1.20185167898973E-16,0.,-1.));
#17392=DIRECTION('ref_axis',(1.,0.,1.20185167898973E-16));
#17393=DIRECTION('',(-1.,0.,-1.20185167898973E-16));
#17394=DIRECTION('',(0.,-1.,0.));
#17395=DIRECTION('',(1.,0.,1.20185167898973E-16));
#17396=DIRECTION('center_axis',(-0.866025403784439,0.,-0.5));
#17397=DIRECTION('ref_axis',(0.5,0.,-0.866025403784439));
#17398=DIRECTION('',(-0.5,0.,0.866025403784439));
#17399=DIRECTION('',(0.,-1.,0.));
#17400=DIRECTION('',(0.5,0.,-0.866025403784439));
#17401=DIRECTION('center_axis',(-0.866025403784439,0.,0.5));
#17402=DIRECTION('ref_axis',(-0.5,0.,-0.866025403784439));
#17403=DIRECTION('',(0.5,0.,0.866025403784439));
#17404=DIRECTION('',(0.,-1.,0.));
#17405=DIRECTION('',(-0.5,0.,-0.866025403784439));
#17406=DIRECTION('center_axis',(-2.40370335797945E-16,0.,1.));
#17407=DIRECTION('ref_axis',(-1.,0.,-2.40370335797945E-16));
#17408=DIRECTION('',(1.,0.,2.40370335797945E-16));
#17409=DIRECTION('',(0.,-1.,0.));
#17410=DIRECTION('',(-1.,0.,-2.40370335797945E-16));
#17411=DIRECTION('center_axis',(0.866025403784439,0.,0.5));
#17412=DIRECTION('ref_axis',(-0.5,0.,0.866025403784439));
#17413=DIRECTION('',(0.5,0.,-0.866025403784439));
#17414=DIRECTION('',(-0.5,0.,0.866025403784439));
#17415=DIRECTION('center_axis',(0.,1.,0.));
#17416=DIRECTION('ref_axis',(1.,0.,0.));
#17417=DIRECTION('center_axis',(0.,-1.,0.));
#17418=DIRECTION('ref_axis',(0.,0.,-1.));
#17419=DIRECTION('center_axis',(0.,1.,0.));
#17420=DIRECTION('ref_axis',(1.,0.,0.));
#17421=DIRECTION('center_axis',(0.,1.,0.));
#17422=DIRECTION('ref_axis',(1.,0.,0.));
#17423=DIRECTION('center_axis',(0.,1.,0.));
#17424=DIRECTION('ref_axis',(0.,0.,1.));
#17425=DIRECTION('center_axis',(0.,-1.,0.));
#17426=DIRECTION('ref_axis',(1.,0.,0.));
#17427=DIRECTION('center_axis',(0.,-1.,0.));
#17428=DIRECTION('ref_axis',(1.,0.,0.));
#17429=DIRECTION('center_axis',(0.,-1.,0.));
#17430=DIRECTION('ref_axis',(1.,0.,0.));
#17431=DIRECTION('',(0.707106781186548,0.707106781186547,8.65956056235493E-17));
#17432=DIRECTION('center_axis',(0.,-1.,0.));
#17433=DIRECTION('ref_axis',(1.,0.,0.));
#17434=DIRECTION('center_axis',(0.,-1.,0.));
#17435=DIRECTION('ref_axis',(1.,0.,0.));
#17436=DIRECTION('',(0.,1.,0.));
#17437=DIRECTION('center_axis',(0.,1.,0.));
#17438=DIRECTION('ref_axis',(1.,0.,0.));
#17439=DIRECTION('center_axis',(0.,-1.,0.));
#17440=DIRECTION('ref_axis',(1.,0.,0.));
#17441=DIRECTION('',(-0.707106781186547,0.707106781186548,-8.65956056235493E-17));
#17442=DIRECTION('center_axis',(0.,-1.,0.));
#17443=DIRECTION('ref_axis',(0.,0.,-1.));
#17444=DIRECTION('center_axis',(0.,-1.,0.));
#17445=DIRECTION('ref_axis',(1.,0.,0.));
#17446=DIRECTION('center_axis',(0.,1.,0.));
#17447=DIRECTION('ref_axis',(1.,0.,0.));
#17448=DIRECTION('center_axis',(0.,1.,0.));
#17449=DIRECTION('ref_axis',(1.,0.,0.));
#17450=DIRECTION('',(-0.447213595499958,0.894427190999916,-5.47678698264203E-17));
#17451=DIRECTION('center_axis',(0.,-1.,0.));
#17452=DIRECTION('ref_axis',(1.,0.,0.));
#17453=DIRECTION('',(0.,1.,0.));
#21346=CARTESIAN_POINT('',(0.,0.,0.));
#21347=CARTESIAN_POINT('Origin',(0.115470053837925,-0.5,-0.2));
#21348=CARTESIAN_POINT('',(0.23094010767585,-0.5,0.));
#21349=CARTESIAN_POINT('',(0.115470053837925,-0.5,-0.2));
#21350=CARTESIAN_POINT('',(0.23094010767585,-0.5,0.));
#21351=CARTESIAN_POINT('',(0.115470053837925,-0.8,-0.2));
#21352=CARTESIAN_POINT('',(0.115470053837925,-0.5,-0.2));
#21353=CARTESIAN_POINT('',(0.23094010767585,-0.8,0.));
#21354=CARTESIAN_POINT('',(0.23094010767585,-0.8,0.));
#21355=CARTESIAN_POINT('',(0.23094010767585,-0.5,0.));
#21356=CARTESIAN_POINT('Origin',(-0.115470053837925,-0.5,-0.2));
#21357=CARTESIAN_POINT('',(-0.115470053837925,-0.5,-0.2));
#21358=CARTESIAN_POINT('',(0.115470053837925,-0.5,-0.2));
#21359=CARTESIAN_POINT('',(-0.115470053837925,-0.8,-0.2));
#21360=CARTESIAN_POINT('',(-0.115470053837925,-0.5,-0.2));
#21361=CARTESIAN_POINT('',(0.115470053837925,-0.8,-0.2));
#21362=CARTESIAN_POINT('Origin',(-0.23094010767585,-0.5,-2.77555756156289E-17));
#21363=CARTESIAN_POINT('',(-0.23094010767585,-0.5,-2.82820063659975E-17));
#21364=CARTESIAN_POINT('',(-0.115470053837925,-0.5,-0.2));
#21365=CARTESIAN_POINT('',(-0.23094010767585,-0.8,-2.77555756156289E-17));
#21366=CARTESIAN_POINT('',(-0.23094010767585,-0.5,-2.82820063659975E-17));
#21367=CARTESIAN_POINT('',(-0.115470053837925,-0.8,-0.2));
#21368=CARTESIAN_POINT('Origin',(-0.115470053837925,-0.5,0.2));
#21369=CARTESIAN_POINT('',(-0.115470053837925,-0.5,0.2));
#21370=CARTESIAN_POINT('',(-0.23094010767585,-0.5,-2.82820063659975E-17));
#21371=CARTESIAN_POINT('',(-0.115470053837925,-0.8,0.2));
#21372=CARTESIAN_POINT('',(-0.115470053837925,-0.5,0.2));
#21373=CARTESIAN_POINT('',(-0.23094010767585,-0.8,-2.82820063659975E-17));
#21374=CARTESIAN_POINT('Origin',(0.115470053837925,-0.5,0.2));
#21375=CARTESIAN_POINT('',(0.115470053837925,-0.5,0.2));
#21376=CARTESIAN_POINT('',(-0.115470053837925,-0.5,0.2));
#21377=CARTESIAN_POINT('',(0.115470053837925,-0.8,0.2));
#21378=CARTESIAN_POINT('',(0.115470053837925,-0.5,0.2));
#21379=CARTESIAN_POINT('',(-0.115470053837925,-0.8,0.2));
#21380=CARTESIAN_POINT('Origin',(0.23094010767585,-0.5,0.));
#21381=CARTESIAN_POINT('',(0.115470053837925,-0.5,0.2));
#21382=CARTESIAN_POINT('',(0.115470053837925,-0.8,0.2));
#21383=CARTESIAN_POINT('Origin',(0.,-0.5,0.));
#21384=CARTESIAN_POINT('Origin',(0.,-0.8,0.));
#21385=CARTESIAN_POINT('Origin',(0.,-1.4,0.));
#21386=CARTESIAN_POINT('',(-0.24505,-1.4,3.00099698131059E-17));
#21387=CARTESIAN_POINT('Origin',(0.,-1.4,0.));
#21388=CARTESIAN_POINT('Origin',(0.375,0.5,0.));
#21389=CARTESIAN_POINT('',(-0.375,0.5,-4.59242549680257E-17));
#21390=CARTESIAN_POINT('Origin',(0.,0.5,0.));
#21391=CARTESIAN_POINT('Origin',(0.,0.475,0.));
#21392=CARTESIAN_POINT('',(-0.425,0.45,-5.20474889637625E-17));
#21393=CARTESIAN_POINT('Origin',(0.,0.45,0.));
#21394=CARTESIAN_POINT('',(-0.4,0.475,-4.89858719658941E-17));
#21395=CARTESIAN_POINT('Origin',(0.,0.24,0.));
#21396=CARTESIAN_POINT('',(-0.425,0.0299999999999998,-5.20474889637625E-17));
#21397=CARTESIAN_POINT('Origin',(0.,0.0299999999999998,0.));
#21398=CARTESIAN_POINT('',(-0.425,0.24,-5.20474889637625E-17));
#21399=CARTESIAN_POINT('Origin',(0.,0.0150000000000001,0.));
#21400=CARTESIAN_POINT('',(-0.395,4.85722573273506E-17,-4.83735485663204E-17));
#21401=CARTESIAN_POINT('Origin',(0.,0.,0.));
#21402=CARTESIAN_POINT('',(-0.41,0.0150000000000001,-5.02105187650415E-17));
#21403=CARTESIAN_POINT('Origin',(0.27,0.,0.));
#21404=CARTESIAN_POINT('',(-0.27,0.,-3.30654635769785E-17));
#21405=CARTESIAN_POINT('Origin',(0.,0.,0.));
#21406=CARTESIAN_POINT('Origin',(0.,-0.02,0.));
#21407=CARTESIAN_POINT('',(-0.24505,-0.0498999999999999,3.00099698131059E-17));
#21408=CARTESIAN_POINT('Origin',(0.,-0.0498999999999999,0.));
#21409=CARTESIAN_POINT('',(-0.26,-0.02,-3.18408167778312E-17));
#21410=CARTESIAN_POINT('Origin',(0.,-0.995,0.));
#21411=CARTESIAN_POINT('',(-0.24505,-0.995,-3.00099698131059E-17));
#57815=UNCERTAINTY_MEASURE_WITH_UNIT(LENGTH_MEASURE(0.001),#57901,
'DISTANCE_ACCURACY_VALUE',
'Maximum model space distance between geometric entities at asserted c
onnectivities');
#57841=UNCERTAINTY_MEASURE_WITH_UNIT(LENGTH_MEASURE(0.001),#57901,
'DISTANCE_ACCURACY_VALUE',
'Maximum model space distance between geometric entities at asserted c
onnectivities');
#57874=(
GEOMETRIC_REPRESENTATION_CONTEXT(3)
GLOBAL_UNCERTAINTY_ASSIGNED_CONTEXT((#57815))
GLOBAL_UNIT_ASSIGNED_CONTEXT((#57901,#57903,#57904))
REPRESENTATION_CONTEXT('','3D')
);
#57900=(
GEOMETRIC_REPRESENTATION_CONTEXT(3)
GLOBAL_UNCERTAINTY_ASSIGNED_CONTEXT((#57841))
GLOBAL_UNIT_ASSIGNED_CONTEXT((#57901,#57903,#57904))
REPRESENTATION_CONTEXT('','3D')
);
#57901=(
LENGTH_UNIT()
NAMED_UNIT(*)
SI_UNIT(.CENTI.,.METRE.)
);
#57903=(
NAMED_UNIT(*)
PLANE_ANGLE_UNIT()
SI_UNIT($,.RADIAN.)
);
#57904=(
NAMED_UNIT(*)
SI_UNIT($,.STERADIAN.)
SOLID_ANGLE_UNIT()
);
#57937=SHAPE_DEFINITION_REPRESENTATION(#58003,#58141);
#58003=PRODUCT_DEFINITION_SHAPE('',$,#58200);
#58141=SHAPE_REPRESENTATION('',(#14883),#57874);
#58167=PRODUCT_DEFINITION_CONTEXT('part definition',#58343,'design');
#58200=PRODUCT_DEFINITION('M5x14 Cap Screw','M5x14 Cap Screw',#58258,#58167);
#58258=PRODUCT_DEFINITION_FORMATION('',$,#58377);
#58343=APPLICATION_CONTEXT(
'Core Data for Automotive Mechanical Design Process');
#58344=PRODUCT_CONTEXT('part definition',#58343,'mechanical');
#58377=PRODUCT('M5x14 Cap Screw','M5x14 Cap Screw','M5x14 Cap Screw',(#58344));
#58466=COLOUR_RGB('Black',0.12,0.14,0.17);
#58467=FILL_AREA_STYLE_COLOUR('',#58466);
#58468=FILL_AREA_STYLE('',(#58467));
#58469=SURFACE_STYLE_FILL_AREA(#58468);
#58470=SURFACE_SIDE_STYLE('',(#58469));
#58471=SURFACE_STYLE_USAGE(.BOTH.,#58470);
#58472=PRESENTATION_STYLE_ASSIGNMENT((#58471));
ENDSEC;
END-ISO-10303-21;
